ISO-10303-21;
HEADER;
/* Generated by software containing ST-Developer
 * from STEP Tools, Inc. (www.steptools.com) 
 */

FILE_DESCRIPTION(
/* description */ ('Round-Shaft Linear Stage with Ball Bushings'),
/* implementation_level */ '2;1');

FILE_NAME(
/* name */ 'M5x14 Cap Screw.step',
/* time_stamp */ '2026-10-27T10:47:55-07:00',
/* author */ (''),
/* organization */ (''),
/* preprocessor_version */ 'ST-DEVELOPER v20.2',
/* originating_system */ 'Autodesk Translation Framework v15.17.0.0',
/* authorisation */ '');

FILE_SCHEMA (('AUTOMOTIVE_DESIGN { 1 0 10303 214 3 1 1 }'));
ENDSEC;

DATA;
#10=MECHANICAL_DESIGN_GEOMETRIC_PRESENTATION_REPRESENTATION('',(#309),#7835);
#235=ORIENTED_CLOSED_SHELL('',*,#4399,.F.);
#239=BREP_WITH_VOIDS('Body1',#4400,(#235));
#245=CONICAL_SURFACE('',#4811,0.4,0.785398163397448);
#246=CONICAL_SURFACE('',#4815,0.41,0.785398163397448);
#247=CONICAL_SURFACE('',#4819,0.26,0.463647609000806);
#267=SHAPE_REPRESENTATION_RELATIONSHIP('SRR','None',#7955,#288);
#288=ADVANCED_BREP_SHAPE_REPRESENTATION('',(#239),#7819);
#309=STYLED_ITEM('',(#8151),#239);
#386=FACE_BOUND('',#1015,.T.);
#511=PLANE('',#4799);
#512=PLANE('',#4800);
#513=PLANE('',#4801);
#514=PLANE('',#4802);
#515=PLANE('',#4803);
#516=PLANE('',#4804);
#517=PLANE('',#4805);
#518=PLANE('',#4806);
#519=PLANE('',#4807);
#520=PLANE('',#4809);
#521=PLANE('',#4817);
#698=FACE_OUTER_BOUND('',#1001,.T.);
#699=FACE_OUTER_BOUND('',#1002,.T.);
#700=FACE_OUTER_BOUND('',#1003,.T.);
#701=FACE_OUTER_BOUND('',#1004,.T.);
#702=FACE_OUTER_BOUND('',#1005,.T.);
#703=FACE_OUTER_BOUND('',#1006,.T.);
#704=FACE_OUTER_BOUND('',#1007,.T.);
#705=FACE_OUTER_BOUND('',#1008,.T.);
#706=FACE_OUTER_BOUND('',#1009,.T.);
#707=FACE_OUTER_BOUND('',#1010,.T.);
#708=FACE_OUTER_BOUND('',#1011,.T.);
#709=FACE_OUTER_BOUND('',#1012,.T.);
#710=FACE_OUTER_BOUND('',#1013,.T.);
#711=FACE_OUTER_BOUND('',#1014,.T.);
#712=FACE_OUTER_BOUND('',#1016,.T.);
#713=FACE_OUTER_BOUND('',#1017,.T.);
#1001=EDGE_LOOP('',(#3374,#3375,#3376,#3377));
#1002=EDGE_LOOP('',(#3378,#3379,#3380,#3381));
#1003=EDGE_LOOP('',(#3382,#3383,#3384,#3385));
#1004=EDGE_LOOP('',(#3386,#3387,#3388,#3389));
#1005=EDGE_LOOP('',(#3390,#3391,#3392,#3393));
#1006=EDGE_LOOP('',(#3394,#3395,#3396,#3397));
#1007=EDGE_LOOP('',(#3398,#3399,#3400,#3401,#3402,#3403));
#1008=EDGE_LOOP('',(#3404,#3405,#3406,#3407,#3408,#3409));
#1009=EDGE_LOOP('',(#3410));
#1010=EDGE_LOOP('',(#3411));
#1011=EDGE_LOOP('',(#3412,#3413,#3414,#3415));
#1012=EDGE_LOOP('',(#3416,#3417,#3418,#3419));
#1013=EDGE_LOOP('',(#3420,#3421,#3422,#3423));
#1014=EDGE_LOOP('',(#3424));
#1015=EDGE_LOOP('',(#3425));
#1016=EDGE_LOOP('',(#3426,#3427,#3428,#3429));
#1017=EDGE_LOOP('',(#3430,#3431,#3432,#3433));
#1381=LINE('',#6981,#1721);
#1382=LINE('',#6983,#1722);
#1383=LINE('',#6985,#1723);
#1384=LINE('',#6986,#1724);
#1385=LINE('',#6989,#1725);
#1386=LINE('',#6991,#1726);
#1387=LINE('',#6992,#1727);
#1388=LINE('',#6995,#1728);
#1389=LINE('',#6997,#1729);
#1390=LINE('',#6998,#1730);
#1391=LINE('',#7001,#1731);
#1392=LINE('',#7003,#1732);
#1393=LINE('',#7004,#1733);
#1394=LINE('',#7007,#1734);
#1395=LINE('',#7009,#1735);
#1396=LINE('',#7010,#1736);
#1397=LINE('',#7012,#1737);
#1398=LINE('',#7013,#1738);
#1399=LINE('',#7025,#1739);
#1400=LINE('',#7029,#1740);
#1401=LINE('',#7033,#1741);
#1402=LINE('',#7040,#1742);
#1403=LINE('',#7042,#1743);
#1721=VECTOR('',#5610,1.);
#1722=VECTOR('',#5611,1.);
#1723=VECTOR('',#5612,1.);
#1724=VECTOR('',#5613,1.);
#1725=VECTOR('',#5616,1.);
#1726=VECTOR('',#5617,1.);
#1727=VECTOR('',#5618,1.);
#1728=VECTOR('',#5621,1.);
#1729=VECTOR('',#5622,1.);
#1730=VECTOR('',#5623,1.);
#1731=VECTOR('',#5626,1.);
#1732=VECTOR('',#5627,1.);
#1733=VECTOR('',#5628,1.);
#1734=VECTOR('',#5631,1.);
#1735=VECTOR('',#5632,1.);
#1736=VECTOR('',#5633,1.);
#1737=VECTOR('',#5636,1.);
#1738=VECTOR('',#5637,1.);
#1739=VECTOR('',#5654,0.4);
#1740=VECTOR('',#5659,0.425);
#1741=VECTOR('',#5664,0.41);
#1742=VECTOR('',#5673,0.26);
#1743=VECTOR('',#5676,0.25);
#1987=CIRCLE('',#4808,0.24505);
#1988=CIRCLE('',#4810,0.375);
#1989=CIRCLE('',#4812,0.425);
#1990=CIRCLE('',#4814,0.425);
#1991=CIRCLE('',#4816,0.395);
#1992=CIRCLE('',#4818,0.27);
#1993=CIRCLE('',#4820,0.24505);
#2244=VERTEX_POINT('',#6979);
#2245=VERTEX_POINT('',#6980);
#2246=VERTEX_POINT('',#6982);
#2247=VERTEX_POINT('',#6984);
#2248=VERTEX_POINT('',#6988);
#2249=VERTEX_POINT('',#6990);
#2250=VERTEX_POINT('',#6994);
#2251=VERTEX_POINT('',#6996);
#2252=VERTEX_POINT('',#7000);
#2253=VERTEX_POINT('',#7002);
#2254=VERTEX_POINT('',#7006);
#2255=VERTEX_POINT('',#7008);
#2256=VERTEX_POINT('',#7017);
#2257=VERTEX_POINT('',#7020);
#2258=VERTEX_POINT('',#7023);
#2259=VERTEX_POINT('',#7027);
#2260=VERTEX_POINT('',#7031);
#2261=VERTEX_POINT('',#7035);
#2262=VERTEX_POINT('',#7038);
#2655=EDGE_CURVE('',#2244,#2245,#1381,.T.);
#2656=EDGE_CURVE('',#2245,#2246,#1382,.T.);
#2657=EDGE_CURVE('',#2246,#2247,#1383,.T.);
#2658=EDGE_CURVE('',#2244,#2247,#1384,.T.);
#2659=EDGE_CURVE('',#2245,#2248,#1385,.T.);
#2660=EDGE_CURVE('',#2248,#2249,#1386,.T.);
#2661=EDGE_CURVE('',#2249,#2246,#1387,.T.);
#2662=EDGE_CURVE('',#2248,#2250,#1388,.T.);
#2663=EDGE_CURVE('',#2250,#2251,#1389,.T.);
#2664=EDGE_CURVE('',#2251,#2249,#1390,.T.);
#2665=EDGE_CURVE('',#2250,#2252,#1391,.T.);
#2666=EDGE_CURVE('',#2252,#2253,#1392,.T.);
#2667=EDGE_CURVE('',#2253,#2251,#1393,.T.);
#2668=EDGE_CURVE('',#2252,#2254,#1394,.T.);
#2669=EDGE_CURVE('',#2254,#2255,#1395,.T.);
#2670=EDGE_CURVE('',#2255,#2253,#1396,.T.);
#2671=EDGE_CURVE('',#2254,#2244,#1397,.T.);
#2672=EDGE_CURVE('',#2247,#2255,#1398,.T.);
#2673=EDGE_CURVE('',#2256,#2256,#1987,.T.);
#2674=EDGE_CURVE('',#2257,#2257,#1988,.T.);
#2675=EDGE_CURVE('',#2258,#2258,#1989,.T.);
#2676=EDGE_CURVE('',#2258,#2257,#1399,.T.);
#2677=EDGE_CURVE('',#2259,#2259,#1990,.T.);
#2678=EDGE_CURVE('',#2259,#2258,#1400,.T.);
#2679=EDGE_CURVE('',#2260,#2260,#1991,.T.);
#2680=EDGE_CURVE('',#2260,#2259,#1401,.T.);
#2681=EDGE_CURVE('',#2261,#2261,#1992,.T.);
#2682=EDGE_CURVE('',#2262,#2262,#1993,.F.);
#2683=EDGE_CURVE('',#2262,#2261,#1402,.T.);
#2684=EDGE_CURVE('',#2256,#2262,#1403,.T.);
#3374=ORIENTED_EDGE('',*,*,#2655,.T.);
#3375=ORIENTED_EDGE('',*,*,#2656,.T.);
#3376=ORIENTED_EDGE('',*,*,#2657,.T.);
#3377=ORIENTED_EDGE('',*,*,#2658,.F.);
#3378=ORIENTED_EDGE('',*,*,#2659,.T.);
#3379=ORIENTED_EDGE('',*,*,#2660,.T.);
#3380=ORIENTED_EDGE('',*,*,#2661,.T.);
#3381=ORIENTED_EDGE('',*,*,#2656,.F.);
#3382=ORIENTED_EDGE('',*,*,#2662,.T.);
#3383=ORIENTED_EDGE('',*,*,#2663,.T.);
#3384=ORIENTED_EDGE('',*,*,#2664,.T.);
#3385=ORIENTED_EDGE('',*,*,#2660,.F.);
#3386=ORIENTED_EDGE('',*,*,#2665,.T.);
#3387=ORIENTED_EDGE('',*,*,#2666,.T.);
#3388=ORIENTED_EDGE('',*,*,#2667,.T.);
#3389=ORIENTED_EDGE('',*,*,#2663,.F.);
#3390=ORIENTED_EDGE('',*,*,#2668,.T.);
#3391=ORIENTED_EDGE('',*,*,#2669,.T.);
#3392=ORIENTED_EDGE('',*,*,#2670,.T.);
#3393=ORIENTED_EDGE('',*,*,#2666,.F.);
#3394=ORIENTED_EDGE('',*,*,#2671,.T.);
#3395=ORIENTED_EDGE('',*,*,#2658,.T.);
#3396=ORIENTED_EDGE('',*,*,#2672,.T.);
#3397=ORIENTED_EDGE('',*,*,#2669,.F.);
#3398=ORIENTED_EDGE('',*,*,#2671,.F.);
#3399=ORIENTED_EDGE('',*,*,#2668,.F.);
#3400=ORIENTED_EDGE('',*,*,#2665,.F.);
#3401=ORIENTED_EDGE('',*,*,#2662,.F.);
#3402=ORIENTED_EDGE('',*,*,#2659,.F.);
#3403=ORIENTED_EDGE('',*,*,#2655,.F.);
#3404=ORIENTED_EDGE('',*,*,#2672,.F.);
#3405=ORIENTED_EDGE('',*,*,#2657,.F.);
#3406=ORIENTED_EDGE('',*,*,#2661,.F.);
#3407=ORIENTED_EDGE('',*,*,#2664,.F.);
#3408=ORIENTED_EDGE('',*,*,#2667,.F.);
#3409=ORIENTED_EDGE('',*,*,#2670,.F.);
#3410=ORIENTED_EDGE('',*,*,#2673,.F.);
#3411=ORIENTED_EDGE('',*,*,#2674,.F.);
#3412=ORIENTED_EDGE('',*,*,#2675,.F.);
#3413=ORIENTED_EDGE('',*,*,#2676,.T.);
#3414=ORIENTED_EDGE('',*,*,#2674,.T.);
#3415=ORIENTED_EDGE('',*,*,#2676,.F.);
#3416=ORIENTED_EDGE('',*,*,#2677,.F.);
#3417=ORIENTED_EDGE('',*,*,#2678,.T.);
#3418=ORIENTED_EDGE('',*,*,#2675,.T.);
#3419=ORIENTED_EDGE('',*,*,#2678,.F.);
#3420=ORIENTED_EDGE('',*,*,#2679,.F.);
#3421=ORIENTED_EDGE('',*,*,#2680,.T.);
#3422=ORIENTED_EDGE('',*,*,#2677,.T.);
#3423=ORIENTED_EDGE('',*,*,#2680,.F.);
#3424=ORIENTED_EDGE('',*,*,#2679,.T.);
#3425=ORIENTED_EDGE('',*,*,#2681,.F.);
#3426=ORIENTED_EDGE('',*,*,#2682,.F.);
#3427=ORIENTED_EDGE('',*,*,#2683,.T.);
#3428=ORIENTED_EDGE('',*,*,#2681,.T.);
#3429=ORIENTED_EDGE('',*,*,#2683,.F.);
#3430=ORIENTED_EDGE('',*,*,#2673,.T.);
#3431=ORIENTED_EDGE('',*,*,#2684,.T.);
#3432=ORIENTED_EDGE('',*,*,#2682,.T.);
#3433=ORIENTED_EDGE('',*,*,#2684,.F.);
#4080=CYLINDRICAL_SURFACE('',#4813,0.425);
#4081=CYLINDRICAL_SURFACE('',#4821,0.24505);
#4217=ADVANCED_FACE('',(#698),#511,.F.);
#4218=ADVANCED_FACE('',(#699),#512,.F.);
#4219=ADVANCED_FACE('',(#700),#513,.F.);
#4220=ADVANCED_FACE('',(#701),#514,.F.);
#4221=ADVANCED_FACE('',(#702),#515,.F.);
#4222=ADVANCED_FACE('',(#703),#516,.F.);
#4223=ADVANCED_FACE('',(#704),#517,.F.);
#4224=ADVANCED_FACE('',(#705),#518,.F.);
#4225=ADVANCED_FACE('',(#706),#519,.F.);
#4226=ADVANCED_FACE('',(#707),#520,.T.);
#4227=ADVANCED_FACE('',(#708),#245,.T.);
#4228=ADVANCED_FACE('',(#709),#4080,.T.);
#4229=ADVANCED_FACE('',(#710),#246,.T.);
#4230=ADVANCED_FACE('',(#711,#386),#521,.T.);
#4231=ADVANCED_FACE('',(#712),#247,.T.);
#4232=ADVANCED_FACE('',(#713),#4081,.T.);
#4399=CLOSED_SHELL('',(#4217,#4218,#4219,#4220,#4221,#4222,#4223,#4224));
#4400=CLOSED_SHELL('',(#4225,#4226,#4227,#4228,#4229,#4230,#4231,#4232));
#4798=AXIS2_PLACEMENT_3D('',#6977,#5606,#5607);
#4799=AXIS2_PLACEMENT_3D('',#6978,#5608,#5609);
#4800=AXIS2_PLACEMENT_3D('',#6987,#5614,#5615);
#4801=AXIS2_PLACEMENT_3D('',#6993,#5619,#5620);
#4802=AXIS2_PLACEMENT_3D('',#6999,#5624,#5625);
#4803=AXIS2_PLACEMENT_3D('',#7005,#5629,#5630);
#4804=AXIS2_PLACEMENT_3D('',#7011,#5634,#5635);
#4805=AXIS2_PLACEMENT_3D('',#7014,#5638,#5639);
#4806=AXIS2_PLACEMENT_3D('',#7015,#5640,#5641);
#4807=AXIS2_PLACEMENT_3D('',#7016,#5642,#5643);
#4808=AXIS2_PLACEMENT_3D('',#7018,#5644,#5645);
#4809=AXIS2_PLACEMENT_3D('',#7019,#5646,#5647);
#4810=AXIS2_PLACEMENT_3D('',#7021,#5648,#5649);
#4811=AXIS2_PLACEMENT_3D('',#7022,#5650,#5651);
#4812=AXIS2_PLACEMENT_3D('',#7024,#5652,#5653);
#4813=AXIS2_PLACEMENT_3D('',#7026,#5655,#5656);
#4814=AXIS2_PLACEMENT_3D('',#7028,#5657,#5658);
#4815=AXIS2_PLACEMENT_3D('',#7030,#5660,#5661);
#4816=AXIS2_PLACEMENT_3D('',#7032,#5662,#5663);
#4817=AXIS2_PLACEMENT_3D('',#7034,#5665,#5666);
#4818=AXIS2_PLACEMENT_3D('',#7036,#5667,#5668);
#4819=AXIS2_PLACEMENT_3D('',#7037,#5669,#5670);
#4820=AXIS2_PLACEMENT_3D('',#7039,#5671,#5672);
#4821=AXIS2_PLACEMENT_3D('',#7041,#5674,#5675);
#5606=DIRECTION('axis',(0.,0.,1.));
#5607=DIRECTION('refdir',(1.,0.,0.));
#5608=DIRECTION('center_axis',(0.866025403784439,0.,-0.5));
#5609=DIRECTION('ref_axis',(0.5,0.,0.866025403784439));
#5610=DIRECTION('',(-0.5,0.,-0.866025403784439));
#5611=DIRECTION('',(0.,-1.,0.));
#5612=DIRECTION('',(0.5,0.,0.866025403784439));
#5613=DIRECTION('',(0.,-1.,0.));
#5614=DIRECTION('center_axis',(1.20185167898973E-16,0.,-1.));
#5615=DIRECTION('ref_axis',(1.,0.,1.20185167898973E-16));
#5616=DIRECTION('',(-1.,0.,-1.20185167898973E-16));
#5617=DIRECTION('',(0.,-1.,0.));
#5618=DIRECTION('',(1.,0.,1.20185167898973E-16));
#5619=DIRECTION('center_axis',(-0.866025403784439,0.,-0.5));
#5620=DIRECTION('ref_axis',(0.5,0.,-0.866025403784439));
#5621=DIRECTION('',(-0.5,0.,0.866025403784439));
#5622=DIRECTION('',(0.,-1.,0.));
#5623=DIRECTION('',(0.5,0.,-0.866025403784439));
#5624=DIRECTION('center_axis',(-0.866025403784439,0.,0.5));
#5625=DIRECTION('ref_axis',(-0.5,0.,-0.866025403784439));
#5626=DIRECTION('',(0.5,0.,0.866025403784439));
#5627=DIRECTION('',(0.,-1.,0.));
#5628=DIRECTION('',(-0.5,0.,-0.866025403784439));
#5629=DIRECTION('center_axis',(-2.40370335797945E-16,0.,1.));
#5630=DIRECTION('ref_axis',(-1.,0.,-2.40370335797945E-16));
#5631=DIRECTION('',(1.,0.,2.40370335797945E-16));
#5632=DIRECTION('',(0.,-1.,0.));
#5633=DIRECTION('',(-1.,0.,-2.40370335797945E-16));
#5634=DIRECTION('center_axis',(0.866025403784439,0.,0.5));
#5635=DIRECTION('ref_axis',(-0.5,0.,0.866025403784439));
#5636=DIRECTION('',(0.5,0.,-0.866025403784439));
#5637=DIRECTION('',(-0.5,0.,0.866025403784439));
#5638=DIRECTION('center_axis',(0.,1.,0.));
#5639=DIRECTION('ref_axis',(1.,0.,0.));
#5640=DIRECTION('center_axis',(0.,-1.,0.));
#5641=DIRECTION('ref_axis',(0.,0.,-1.));
#5642=DIRECTION('center_axis',(0.,1.,0.));
#5643=DIRECTION('ref_axis',(1.,0.,0.));
#5644=DIRECTION('center_axis',(0.,1.,0.));
#5645=DIRECTION('ref_axis',(1.,0.,0.));
#5646=DIRECTION('center_axis',(0.,1.,0.));
#5647=DIRECTION('ref_axis',(0.,0.,1.));
#5648=DIRECTION('center_axis',(0.,-1.,0.));
#5649=DIRECTION('ref_axis',(1.,0.,0.));
#5650=DIRECTION('center_axis',(0.,-1.,0.));
#5651=DIRECTION('ref_axis',(1.,0.,0.));
#5652=DIRECTION('center_axis',(0.,-1.,0.));
#5653=DIRECTION('ref_axis',(1.,0.,0.));
#5654=DIRECTION('',(0.707106781186548,0.707106781186547,8.65956056235493E-17));
#5655=DIRECTION('center_axis',(0.,-1.,0.));
#5656=DIRECTION('ref_axis',(1.,0.,0.));
#5657=DIRECTION('center_axis',(0.,-1.,0.));
#5658=DIRECTION('ref_axis',(1.,0.,0.));
#5659=DIRECTION('',(0.,1.,0.));
#5660=DIRECTION('center_axis',(0.,1.,0.));
#5661=DIRECTION('ref_axis',(1.,0.,0.));
#5662=DIRECTION('center_axis',(0.,-1.,0.));
#5663=DIRECTION('ref_axis',(1.,0.,0.));
#5664=DIRECTION('',(-0.707106781186547,0.707106781186548,-8.65956056235493E-17));
#5665=DIRECTION('center_axis',(0.,-1.,0.));
#5666=DIRECTION('ref_axis',(0.,0.,-1.));
#5667=DIRECTION('center_axis',(0.,-1.,0.));
#5668=DIRECTION('ref_axis',(1.,0.,0.));
#5669=DIRECTION('center_axis',(0.,1.,0.));
#5670=DIRECTION('ref_axis',(1.,0.,0.));
#5671=DIRECTION('center_axis',(0.,1.,0.));
#5672=DIRECTION('ref_axis',(1.,0.,0.));
#5673=DIRECTION('',(-0.447213595499958,0.894427190999916,-5.47678698264203E-17));
#5674=DIRECTION('center_axis',(0.,-1.,0.));
#5675=DIRECTION('ref_axis',(1.,0.,0.));
#5676=DIRECTION('',(0.,1.,0.));
#6977=CARTESIAN_POINT('',(0.,0.,0.));
#6978=CARTESIAN_POINT('Origin',(0.115470053837925,-0.5,-0.2));
#6979=CARTESIAN_POINT('',(0.23094010767585,-0.5,0.));
#6980=CARTESIAN_POINT('',(0.115470053837925,-0.5,-0.2));
#6981=CARTESIAN_POINT('',(0.23094010767585,-0.5,0.));
#6982=CARTESIAN_POINT('',(0.115470053837925,-0.8,-0.2));
#6983=CARTESIAN_POINT('',(0.115470053837925,-0.5,-0.2));
#6984=CARTESIAN_POINT('',(0.23094010767585,-0.8,0.));
#6985=CARTESIAN_POINT('',(0.23094010767585,-0.8,0.));
#6986=CARTESIAN_POINT('',(0.23094010767585,-0.5,0.));
#6987=CARTESIAN_POINT('Origin',(-0.115470053837925,-0.5,-0.2));
#6988=CARTESIAN_POINT('',(-0.115470053837925,-0.5,-0.2));
#6989=CARTESIAN_POINT('',(0.115470053837925,-0.5,-0.2));
#6990=CARTESIAN_POINT('',(-0.115470053837925,-0.8,-0.2));
#6991=CARTESIAN_POINT('',(-0.115470053837925,-0.5,-0.2));
#6992=CARTESIAN_POINT('',(0.115470053837925,-0.8,-0.2));
#6993=CARTESIAN_POINT('Origin',(-0.23094010767585,-0.5,-2.77555756156289E-17));
#6994=CARTESIAN_POINT('',(-0.23094010767585,-0.5,-2.82820063659975E-17));
#6995=CARTESIAN_POINT('',(-0.115470053837925,-0.5,-0.2));
#6996=CARTESIAN_POINT('',(-0.23094010767585,-0.8,-2.77555756156289E-17));
#6997=CARTESIAN_POINT('',(-0.23094010767585,-0.5,-2.82820063659975E-17));
#6998=CARTESIAN_POINT('',(-0.115470053837925,-0.8,-0.2));
#6999=CARTESIAN_POINT('Origin',(-0.115470053837925,-0.5,0.2));
#7000=CARTESIAN_POINT('',(-0.115470053837925,-0.5,0.2));
#7001=CARTESIAN_POINT('',(-0.23094010767585,-0.5,-2.82820063659975E-17));
#7002=CARTESIAN_POINT('',(-0.115470053837925,-0.8,0.2));
#7003=CARTESIAN_POINT('',(-0.115470053837925,-0.5,0.2));
#7004=CARTESIAN_POINT('',(-0.23094010767585,-0.8,-2.82820063659975E-17));
#7005=CARTESIAN_POINT('Origin',(0.115470053837925,-0.5,0.2));
#7006=CARTESIAN_POINT('',(0.115470053837925,-0.5,0.2));
#7007=CARTESIAN_POINT('',(-0.115470053837925,-0.5,0.2));
#7008=CARTESIAN_POINT('',(0.115470053837925,-0.8,0.2));
#7009=CARTESIAN_POINT('',(0.115470053837925,-0.5,0.2));
#7010=CARTESIAN_POINT('',(-0.115470053837925,-0.8,0.2));
#7011=CARTESIAN_POINT('Origin',(0.23094010767585,-0.5,0.));
#7012=CARTESIAN_POINT('',(0.115470053837925,-0.5,0.2));
#7013=CARTESIAN_POINT('',(0.115470053837925,-0.8,0.2));
#7014=CARTESIAN_POINT('Origin',(0.,-0.5,0.));
#7015=CARTESIAN_POINT('Origin',(0.,-0.8,0.));
#7016=CARTESIAN_POINT('Origin',(0.,-1.4,0.));
#7017=CARTESIAN_POINT('',(-0.24505,-1.4,3.00099698131059E-17));
#7018=CARTESIAN_POINT('Origin',(0.,-1.4,0.));
#7019=CARTESIAN_POINT('Origin',(0.375,0.5,0.));
#7020=CARTESIAN_POINT('',(-0.375,0.5,-4.59242549680257E-17));
#7021=CARTESIAN_POINT('Origin',(0.,0.5,0.));
#7022=CARTESIAN_POINT('Origin',(0.,0.475,0.));
#7023=CARTESIAN_POINT('',(-0.425,0.45,-5.20474889637625E-17));
#7024=CARTESIAN_POINT('Origin',(0.,0.45,0.));
#7025=CARTESIAN_POINT('',(-0.4,0.475,-4.89858719658941E-17));
#7026=CARTESIAN_POINT('Origin',(0.,0.24,0.));
#7027=CARTESIAN_POINT('',(-0.425,0.0299999999999998,-5.20474889637625E-17));
#7028=CARTESIAN_POINT('Origin',(0.,0.0299999999999998,0.));
#7029=CARTESIAN_POINT('',(-0.425,0.24,-5.20474889637625E-17));
#7030=CARTESIAN_POINT('Origin',(0.,0.0150000000000001,0.));
#7031=CARTESIAN_POINT('',(-0.395,4.85722573273506E-17,-4.83735485663204E-17));
#7032=CARTESIAN_POINT('Origin',(0.,0.,0.));
#7033=CARTESIAN_POINT('',(-0.41,0.0150000000000001,-5.02105187650415E-17));
#7034=CARTESIAN_POINT('Origin',(0.27,0.,0.));
#7035=CARTESIAN_POINT('',(-0.27,0.,-3.30654635769785E-17));
#7036=CARTESIAN_POINT('Origin',(0.,0.,0.));
#7037=CARTESIAN_POINT('Origin',(0.,-0.02,0.));
#7038=CARTESIAN_POINT('',(-0.24505,-0.0498999999999999,3.00099698131059E-17));
#7039=CARTESIAN_POINT('Origin',(0.,-0.0498999999999999,0.));
#7040=CARTESIAN_POINT('',(-0.26,-0.02,-3.18408167778312E-17));
#7041=CARTESIAN_POINT('Origin',(0.,-0.995,0.));
#7042=CARTESIAN_POINT('',(-0.24505,-0.995,-3.00099698131059E-17));
#7793=UNCERTAINTY_MEASURE_WITH_UNIT(LENGTH_MEASURE(0.001),#7836,
'DISTANCE_ACCURACY_VALUE',
'Maximum model space distance between geometric entities at asserted c
onnectivities');
#7809=UNCERTAINTY_MEASURE_WITH_UNIT(LENGTH_MEASURE(0.001),#7836,
'DISTANCE_ACCURACY_VALUE',
'Maximum model space distance between geometric entities at asserted c
onnectivities');
#7819=(
GEOMETRIC_REPRESENTATION_CONTEXT(3)
GLOBAL_UNCERTAINTY_ASSIGNED_CONTEXT((#7793))
GLOBAL_UNIT_ASSIGNED_CONTEXT((#7836,#7838,#7839))
REPRESENTATION_CONTEXT('','3D')
);
#7835=(
GEOMETRIC_REPRESENTATION_CONTEXT(3)
GLOBAL_UNCERTAINTY_ASSIGNED_CONTEXT((#7809))
GLOBAL_UNIT_ASSIGNED_CONTEXT((#7836,#7838,#7839))
REPRESENTATION_CONTEXT('','3D')
);
#7836=(
LENGTH_UNIT()
NAMED_UNIT(*)
SI_UNIT(.CENTI.,.METRE.)
);
#7838=(
NAMED_UNIT(*)
PLANE_ANGLE_UNIT()
SI_UNIT($,.RADIAN.)
);
#7839=(
NAMED_UNIT(*)
SI_UNIT($,.STERADIAN.)
SOLID_ANGLE_UNIT()
);
#7849=SHAPE_DEFINITION_REPRESENTATION(#7874,#7955);
#7874=PRODUCT_DEFINITION_SHAPE('',$,#7981);
#7955=SHAPE_REPRESENTATION('',(#4798),#7819);
#7971=PRODUCT_DEFINITION_CONTEXT('part definition',#8048,'design');
#7981=PRODUCT_DEFINITION('M5x14 Cap Screw','M5x14 Cap Screw',#8006,#7971);
#8006=PRODUCT_DEFINITION_FORMATION('',$,#8059);
#8048=APPLICATION_CONTEXT(
'Core Data for Automotive Mechanical Design Process');
#8049=PRODUCT_CONTEXT('part definition',#8048,'mechanical');
#8059=PRODUCT('M5x14 Cap Screw','M5x14 Cap Screw','M5x14 Cap Screw',(#8049));
#8145=COLOUR_RGB('Black',0.12,0.14,0.17);
#8146=FILL_AREA_STYLE_COLOUR('',#8145);
#8147=FILL_AREA_STYLE('',(#8146));
#8148=SURFACE_STYLE_FILL_AREA(#8147);
#8149=SURFACE_SIDE_STYLE('',(#8148));
#8150=SURFACE_STYLE_USAGE(.BOTH.,#8149);
#8151=PRESENTATION_STYLE_ASSIGNMENT((#8150));
ENDSEC;
END-ISO-10303-21;
